ISO-10303-21;
HEADER;
/* Generated by software containing ST-Developer
 * from STEP Tools, Inc. (www.steptools.com) 
 */

FILE_DESCRIPTION(
/* description */ (''),
/* implementation_level */ '2;1');

FILE_NAME(
/* name */ 'M5x14 Steel 4.6 Plain v1 (3).step',
/* time_stamp */ '2026-10-23T22:29:29+06:00',
/* author */ (''),
/* organization */ (''),
/* preprocessor_version */ 'ST-DEVELOPER v20.2',
/* originating_system */ 'Autodesk Translation Framework v15.15.0.0',
/* authorisation */ '');

FILE_SCHEMA (('AUTOMOTIVE_DESIGN { 1 0 10303 214 3 1 1 }'));
ENDSEC;

DATA;
#10=MECHANICAL_DESIGN_GEOMETRIC_PRESENTATION_REPRESENTATION('',(#75),#7047);
#55=SHAPE_REPRESENTATION_RELATIONSHIP('SRR','None',#7088,#65);
#65=ADVANCED_BREP_SHAPE_REPRESENTATION('',(#88),#7040);
#75=STYLED_ITEM('',(#7212),#88);
#88=MANIFOLD_SOLID_BREP('Body1',#3400);
#98=SPHERICAL_SURFACE('',#3758,12.8319377609308);
#105=CONICAL_SURFACE('',#3753,2.33923048454133,0.261799387799147);
#106=CONICAL_SURFACE('',#3762,5.05813690328693,0.0872664626099692);
#110=FACE_BOUND('',#552,.T.);
#128=TOROIDAL_SURFACE('',#3745,2.37846096908266,0.2);
#174=PLANE('',#3707);
#175=PLANE('',#3709);
#176=PLANE('',#3712);
#177=PLANE('',#3717);
#178=PLANE('',#3719);
#179=PLANE('',#3722);
#180=PLANE('',#3728);
#181=PLANE('',#3733);
#182=PLANE('',#3735);
#183=PLANE('',#3737);
#184=PLANE('',#3740);
#185=PLANE('',#3742);
#186=PLANE('',#3744);
#187=PLANE('',#3749);
#188=PLANE('',#3757);
#341=FACE_OUTER_BOUND('',#533,.T.);
#342=FACE_OUTER_BOUND('',#534,.T.);
#343=FACE_OUTER_BOUND('',#535,.T.);
#344=FACE_OUTER_BOUND('',#536,.T.);
#345=FACE_OUTER_BOUND('',#537,.T.);
#346=FACE_OUTER_BOUND('',#538,.T.);
#347=FACE_OUTER_BOUND('',#539,.T.);
#348=FACE_OUTER_BOUND('',#540,.T.);
#349=FACE_OUTER_BOUND('',#541,.T.);
#350=FACE_OUTER_BOUND('',#542,.T.);
#351=FACE_OUTER_BOUND('',#543,.T.);
#352=FACE_OUTER_BOUND('',#544,.T.);
#353=FACE_OUTER_BOUND('',#545,.T.);
#354=FACE_OUTER_BOUND('',#546,.T.);
#355=FACE_OUTER_BOUND('',#547,.T.);
#356=FACE_OUTER_BOUND('',#548,.T.);
#357=FACE_OUTER_BOUND('',#549,.T.);
#358=FACE_OUTER_BOUND('',#550,.T.);
#359=FACE_OUTER_BOUND('',#551,.T.);
#360=FACE_OUTER_BOUND('',#553,.T.);
#361=FACE_OUTER_BOUND('',#554,.T.);
#362=FACE_OUTER_BOUND('',#555,.T.);
#363=FACE_OUTER_BOUND('',#556,.T.);
#364=FACE_OUTER_BOUND('',#557,.T.);
#365=FACE_OUTER_BOUND('',#558,.T.);
#533=EDGE_LOOP('',(#2599,#2600,#2601,#2602,#2603,#2604));
#534=EDGE_LOOP('',(#2605,#2606,#2607));
#535=EDGE_LOOP('',(#2608,#2609,#2610,#2611,#2612,#2613));
#536=EDGE_LOOP('',(#2614,#2615,#2616));
#537=EDGE_LOOP('',(#2617,#2618,#2619,#2620,#2621,#2622));
#538=EDGE_LOOP('',(#2623,#2624,#2625));
#539=EDGE_LOOP('',(#2626,#2627,#2628,#2629,#2630,#2631));
#540=EDGE_LOOP('',(#2632,#2633,#2634));
#541=EDGE_LOOP('',(#2635,#2636,#2637,#2638,#2639,#2640));
#542=EDGE_LOOP('',(#2641,#2642,#2643));
#543=EDGE_LOOP('',(#2644,#2645,#2646,#2647,#2648,#2649));
#544=EDGE_LOOP('',(#2650,#2651,#2652));
#545=EDGE_LOOP('',(#2653,#2654,#2655));
#546=EDGE_LOOP('',(#2656,#2657,#2658,#2659,#2660,#2661,#2662));
#547=EDGE_LOOP('',(#2663,#2664,#2665));
#548=EDGE_LOOP('',(#2666,#2667,#2668,#2669,#2670,#2671));
#549=EDGE_LOOP('',(#2672,#2673,#2674,#2675,#2676,#2677,#2678,#2679));
#550=EDGE_LOOP('',(#2680,#2681,#2682,#2683));
#551=EDGE_LOOP('',(#2684));
#552=EDGE_LOOP('',(#2685));
#553=EDGE_LOOP('',(#2686,#2687,#2688,#2689));
#554=EDGE_LOOP('',(#2690,#2691,#2692,#2693));
#555=EDGE_LOOP('',(#2694,#2695,#2696,#2697));
#556=EDGE_LOOP('',(#2698));
#557=EDGE_LOOP('',(#2699,#2700,#2701,#2702,#2703,#2704,#2705,#2706,#2707,
#2708,#2709,#2710,#2711,#2712,#2713,#2714,#2715,#2716,#2717,#2718,#2719));
#558=EDGE_LOOP('',(#2720,#2721,#2722,#2723,#2724));
#743=CIRCLE('',#3705,0.946);
#744=CIRCLE('',#3708,12.8232171353527);
#745=CIRCLE('',#3710,12.1073709048319);
#746=CIRCLE('',#3713,12.8232171353527);
#747=CIRCLE('',#3715,0.946);
#748=CIRCLE('',#3718,12.8232171353527);
#749=CIRCLE('',#3720,12.1073709048319);
#750=CIRCLE('',#3723,12.8232171353527);
#751=CIRCLE('',#3726,0.946);
#752=CIRCLE('',#3729,12.8232171353527);
#753=CIRCLE('',#3731,0.946);
#754=CIRCLE('',#3734,12.8232171353527);
#755=CIRCLE('',#3736,12.8232171353527);
#756=CIRCLE('',#3738,12.1073709048319);
#757=CIRCLE('',#3739,12.1073709048319);
#758=CIRCLE('',#3741,12.8232171353527);
#759=CIRCLE('',#3743,12.1073709048319);
#760=CIRCLE('',#3746,2.37846096908266);
#761=CIRCLE('',#3747,0.2);
#762=CIRCLE('',#3748,2.17846096908266);
#763=CIRCLE('',#3750,5.15);
#764=CIRCLE('',#3752,2.17846096908266);
#765=CIRCLE('',#3754,2.4505);
#766=CIRCLE('',#3756,2.4505);
#767=CIRCLE('',#3759,12.8319377609308);
#768=CIRCLE('',#3760,4.96627380657387);
#769=CIRCLE('',#3761,4.96627380657387);
#819=ELLIPSE('',#3704,1.892,0.946);
#820=ELLIPSE('',#3706,1.892,0.946);
#821=ELLIPSE('',#3711,1.892,0.946);
#822=ELLIPSE('',#3716,1.892,0.946);
#823=ELLIPSE('',#3721,1.892,0.946);
#824=ELLIPSE('',#3725,1.892,0.946);
#825=ELLIPSE('',#3727,1.892,0.946);
#826=ELLIPSE('',#3732,1.892,0.946);
#899=LINE('',#5513,#1193);
#900=LINE('',#5520,#1194);
#901=LINE('',#5524,#1195);
#902=LINE('',#5529,#1196);
#903=LINE('',#5532,#1197);
#904=LINE('',#5536,#1198);
#905=LINE('',#5558,#1199);
#906=LINE('',#5562,#1200);
#907=LINE('',#5567,#1201);
#908=LINE('',#5570,#1202);
#909=LINE('',#5574,#1203);
#910=LINE('',#5594,#1204);
#911=LINE('',#5601,#1205);
#912=LINE('',#5605,#1206);
#913=LINE('',#5627,#1207);
#914=LINE('',#5631,#1208);
#915=LINE('',#5635,#1209);
#916=LINE('',#5639,#1210);
#917=LINE('',#5644,#1211);
#918=LINE('',#5647,#1212);
#919=LINE('',#5661,#1213);
#920=LINE('',#5665,#1214);
#921=LINE('',#5669,#1215);
#922=LINE('',#5678,#1216);
#1193=VECTOR('',#4336,10.);
#1194=VECTOR('',#4343,10.);
#1195=VECTOR('',#4348,10.);
#1196=VECTOR('',#4353,10.);
#1197=VECTOR('',#4356,10.);
#1198=VECTOR('',#4361,10.);
#1199=VECTOR('',#4368,10.);
#1200=VECTOR('',#4373,10.);
#1201=VECTOR('',#4378,10.);
#1202=VECTOR('',#4381,10.);
#1203=VECTOR('',#4386,10.);
#1204=VECTOR('',#4389,10.);
#1205=VECTOR('',#4396,10.);
#1206=VECTOR('',#4401,10.);
#1207=VECTOR('',#4408,10.);
#1208=VECTOR('',#4413,10.);
#1209=VECTOR('',#4418,10.);
#1210=VECTOR('',#4423,10.);
#1211=VECTOR('',#4430,10.);
#1212=VECTOR('',#4435,10.);
#1213=VECTOR('',#4454,2.17846096908266);
#1214=VECTOR('',#4459,2.33923048454133);
#1215=VECTOR('',#4464,2.5);
#1216=VECTOR('',#4477,5.05813690328693);
#1427=B_SPLINE_CURVE_WITH_KNOTS('',3,(#5497,#5498,#5499,#5500,#5501,#5502,
#5503,#5504,#5505,#5506,#5507,#5508,#5509,#5510,#5511),.UNSPECIFIED.,.F.,
 .F.,(4,2,2,3,2,2,4),(-0.0714521071173775,-0.0712222400952786,-0.0356111200476392,
0.,0.0356111200476392,0.0712222400952784,0.0714521071173274),
 .UNSPECIFIED.);
#1428=B_SPLINE_CURVE_WITH_KNOTS('',3,(#5539,#5540,#5541,#5542,#5543,#5544,
#5545,#5546,#5547,#5548,#5549,#5550,#5551,#5552,#5553),.UNSPECIFIED.,.F.,
 .F.,(4,2,2,3,2,2,4),(-0.071452107117379,-0.0712222400952786,-0.0356111200476392,
0.,0.0356111200476392,0.0712222400952784,0.071452107117329),
 .UNSPECIFIED.);
#1429=B_SPLINE_CURVE_WITH_KNOTS('',3,(#5578,#5579,#5580,#5581,#5582,#5583,
#5584,#5585,#5586,#5587,#5588,#5589,#5590,#5591,#5592),.UNSPECIFIED.,.F.,
 .F.,(4,2,2,3,2,2,4),(-0.0714521071173781,-0.0712222400952784,-0.0356111200476392,
0.,0.0356111200476392,0.0712222400952785,0.0714521071173282),
 .UNSPECIFIED.);
#1430=B_SPLINE_CURVE_WITH_KNOTS('',3,(#5608,#5609,#5610,#5611,#5612,#5613,
#5614,#5615,#5616,#5617,#5618,#5619,#5620,#5621,#5622),.UNSPECIFIED.,.F.,
 .F.,(4,2,2,3,2,2,4),(-0.0714521071173768,-0.0712222400952786,-0.0356111200476392,
0.,0.0356111200476392,0.0712222400952785,0.0714521071173268),
 .UNSPECIFIED.);
#1555=VERTEX_POINT('',#5495);
#1556=VERTEX_POINT('',#5496);
#1557=VERTEX_POINT('',#5512);
#1558=VERTEX_POINT('',#5514);
#1559=VERTEX_POINT('',#5516);
#1560=VERTEX_POINT('',#5518);
#1561=VERTEX_POINT('',#5522);
#1562=VERTEX_POINT('',#5526);
#1563=VERTEX_POINT('',#5528);
#1564=VERTEX_POINT('',#5530);
#1565=VERTEX_POINT('',#5534);
#1566=VERTEX_POINT('',#5538);
#1567=VERTEX_POINT('',#5554);
#1568=VERTEX_POINT('',#5556);
#1569=VERTEX_POINT('',#5560);
#1570=VERTEX_POINT('',#5564);
#1571=VERTEX_POINT('',#5566);
#1572=VERTEX_POINT('',#5568);
#1573=VERTEX_POINT('',#5572);
#1574=VERTEX_POINT('',#5576);
#1575=VERTEX_POINT('',#5577);
#1576=VERTEX_POINT('',#5593);
#1577=VERTEX_POINT('',#5595);
#1578=VERTEX_POINT('',#5597);
#1579=VERTEX_POINT('',#5599);
#1580=VERTEX_POINT('',#5603);
#1581=VERTEX_POINT('',#5607);
#1582=VERTEX_POINT('',#5623);
#1583=VERTEX_POINT('',#5625);
#1584=VERTEX_POINT('',#5629);
#1585=VERTEX_POINT('',#5633);
#1586=VERTEX_POINT('',#5637);
#1587=VERTEX_POINT('',#5642);
#1588=VERTEX_POINT('',#5650);
#1589=VERTEX_POINT('',#5652);
#1590=VERTEX_POINT('',#5656);
#1591=VERTEX_POINT('',#5659);
#1592=VERTEX_POINT('',#5663);
#1593=VERTEX_POINT('',#5667);
#1594=VERTEX_POINT('',#5672);
#1595=VERTEX_POINT('',#5674);
#1934=EDGE_CURVE('',#1555,#1556,#1427,.T.);
#1935=EDGE_CURVE('',#1557,#1555,#899,.T.);
#1936=EDGE_CURVE('',#1557,#1558,#819,.F.);
#1937=EDGE_CURVE('',#1558,#1559,#743,.F.);
#1938=EDGE_CURVE('',#1560,#1559,#820,.T.);
#1939=EDGE_CURVE('',#1556,#1560,#900,.T.);
#1940=EDGE_CURVE('',#1556,#1561,#744,.T.);
#1941=EDGE_CURVE('',#1561,#1560,#901,.F.);
#1942=EDGE_CURVE('',#1561,#1562,#745,.T.);
#1943=EDGE_CURVE('',#1559,#1563,#902,.F.);
#1944=EDGE_CURVE('',#1564,#1563,#821,.F.);
#1945=EDGE_CURVE('',#1562,#1564,#903,.T.);
#1946=EDGE_CURVE('',#1562,#1565,#746,.T.);
#1947=EDGE_CURVE('',#1564,#1565,#904,.T.);
#1948=EDGE_CURVE('',#1565,#1566,#1428,.T.);
#1949=EDGE_CURVE('',#1563,#1567,#747,.F.);
#1950=EDGE_CURVE('',#1568,#1567,#822,.T.);
#1951=EDGE_CURVE('',#1566,#1568,#905,.T.);
#1952=EDGE_CURVE('',#1566,#1569,#748,.T.);
#1953=EDGE_CURVE('',#1569,#1568,#906,.F.);
#1954=EDGE_CURVE('',#1569,#1570,#749,.T.);
#1955=EDGE_CURVE('',#1567,#1571,#907,.F.);
#1956=EDGE_CURVE('',#1572,#1571,#823,.F.);
#1957=EDGE_CURVE('',#1570,#1572,#908,.T.);
#1958=EDGE_CURVE('',#1570,#1573,#750,.T.);
#1959=EDGE_CURVE('',#1572,#1573,#909,.T.);
#1960=EDGE_CURVE('',#1574,#1575,#1429,.T.);
#1961=EDGE_CURVE('',#1576,#1574,#910,.T.);
#1962=EDGE_CURVE('',#1576,#1577,#824,.F.);
#1963=EDGE_CURVE('',#1577,#1578,#751,.F.);
#1964=EDGE_CURVE('',#1579,#1578,#825,.T.);
#1965=EDGE_CURVE('',#1575,#1579,#911,.T.);
#1966=EDGE_CURVE('',#1575,#1580,#752,.T.);
#1967=EDGE_CURVE('',#1580,#1579,#912,.F.);
#1968=EDGE_CURVE('',#1573,#1581,#1430,.T.);
#1969=EDGE_CURVE('',#1571,#1582,#753,.F.);
#1970=EDGE_CURVE('',#1583,#1582,#826,.T.);
#1971=EDGE_CURVE('',#1581,#1583,#913,.T.);
#1972=EDGE_CURVE('',#1581,#1584,#754,.T.);
#1973=EDGE_CURVE('',#1584,#1583,#914,.F.);
#1974=EDGE_CURVE('',#1585,#1555,#755,.T.);
#1975=EDGE_CURVE('',#1585,#1557,#915,.T.);
#1976=EDGE_CURVE('',#1580,#1586,#756,.T.);
#1977=EDGE_CURVE('',#1578,#1558,#916,.F.);
#1978=EDGE_CURVE('',#1586,#1585,#757,.T.);
#1979=EDGE_CURVE('',#1587,#1574,#758,.T.);
#1980=EDGE_CURVE('',#1587,#1576,#917,.T.);
#1981=EDGE_CURVE('',#1584,#1587,#759,.T.);
#1982=EDGE_CURVE('',#1582,#1577,#918,.F.);
#1983=EDGE_CURVE('',#1588,#1588,#760,.T.);
#1984=EDGE_CURVE('',#1588,#1589,#761,.T.);
#1985=EDGE_CURVE('',#1589,#1589,#762,.T.);
#1986=EDGE_CURVE('',#1590,#1590,#763,.T.);
#1987=EDGE_CURVE('',#1591,#1591,#764,.T.);
#1988=EDGE_CURVE('',#1591,#1589,#919,.T.);
#1989=EDGE_CURVE('',#1592,#1592,#765,.T.);
#1990=EDGE_CURVE('',#1592,#1591,#920,.T.);
#1991=EDGE_CURVE('',#1593,#1593,#766,.F.);
#1992=EDGE_CURVE('',#1593,#1592,#921,.T.);
#1993=EDGE_CURVE('',#1586,#1594,#767,.T.);
#1994=EDGE_CURVE('',#1595,#1594,#768,.T.);
#1995=EDGE_CURVE('',#1594,#1595,#769,.T.);
#1996=EDGE_CURVE('',#1590,#1595,#922,.T.);
#2599=ORIENTED_EDGE('',*,*,#1934,.F.);
#2600=ORIENTED_EDGE('',*,*,#1935,.F.);
#2601=ORIENTED_EDGE('',*,*,#1936,.T.);
#2602=ORIENTED_EDGE('',*,*,#1937,.T.);
#2603=ORIENTED_EDGE('',*,*,#1938,.F.);
#2604=ORIENTED_EDGE('',*,*,#1939,.F.);
#2605=ORIENTED_EDGE('',*,*,#1940,.F.);
#2606=ORIENTED_EDGE('',*,*,#1939,.T.);
#2607=ORIENTED_EDGE('',*,*,#1941,.F.);
#2608=ORIENTED_EDGE('',*,*,#1942,.F.);
#2609=ORIENTED_EDGE('',*,*,#1941,.T.);
#2610=ORIENTED_EDGE('',*,*,#1938,.T.);
#2611=ORIENTED_EDGE('',*,*,#1943,.T.);
#2612=ORIENTED_EDGE('',*,*,#1944,.F.);
#2613=ORIENTED_EDGE('',*,*,#1945,.F.);
#2614=ORIENTED_EDGE('',*,*,#1946,.F.);
#2615=ORIENTED_EDGE('',*,*,#1945,.T.);
#2616=ORIENTED_EDGE('',*,*,#1947,.T.);
#2617=ORIENTED_EDGE('',*,*,#1948,.F.);
#2618=ORIENTED_EDGE('',*,*,#1947,.F.);
#2619=ORIENTED_EDGE('',*,*,#1944,.T.);
#2620=ORIENTED_EDGE('',*,*,#1949,.T.);
#2621=ORIENTED_EDGE('',*,*,#1950,.F.);
#2622=ORIENTED_EDGE('',*,*,#1951,.F.);
#2623=ORIENTED_EDGE('',*,*,#1952,.F.);
#2624=ORIENTED_EDGE('',*,*,#1951,.T.);
#2625=ORIENTED_EDGE('',*,*,#1953,.F.);
#2626=ORIENTED_EDGE('',*,*,#1954,.F.);
#2627=ORIENTED_EDGE('',*,*,#1953,.T.);
#2628=ORIENTED_EDGE('',*,*,#1950,.T.);
#2629=ORIENTED_EDGE('',*,*,#1955,.T.);
#2630=ORIENTED_EDGE('',*,*,#1956,.F.);
#2631=ORIENTED_EDGE('',*,*,#1957,.F.);
#2632=ORIENTED_EDGE('',*,*,#1958,.F.);
#2633=ORIENTED_EDGE('',*,*,#1957,.T.);
#2634=ORIENTED_EDGE('',*,*,#1959,.T.);
#2635=ORIENTED_EDGE('',*,*,#1960,.F.);
#2636=ORIENTED_EDGE('',*,*,#1961,.F.);
#2637=ORIENTED_EDGE('',*,*,#1962,.T.);
#2638=ORIENTED_EDGE('',*,*,#1963,.T.);
#2639=ORIENTED_EDGE('',*,*,#1964,.F.);
#2640=ORIENTED_EDGE('',*,*,#1965,.F.);
#2641=ORIENTED_EDGE('',*,*,#1966,.F.);
#2642=ORIENTED_EDGE('',*,*,#1965,.T.);
#2643=ORIENTED_EDGE('',*,*,#1967,.F.);
#2644=ORIENTED_EDGE('',*,*,#1968,.F.);
#2645=ORIENTED_EDGE('',*,*,#1959,.F.);
#2646=ORIENTED_EDGE('',*,*,#1956,.T.);
#2647=ORIENTED_EDGE('',*,*,#1969,.T.);
#2648=ORIENTED_EDGE('',*,*,#1970,.F.);
#2649=ORIENTED_EDGE('',*,*,#1971,.F.);
#2650=ORIENTED_EDGE('',*,*,#1972,.F.);
#2651=ORIENTED_EDGE('',*,*,#1971,.T.);
#2652=ORIENTED_EDGE('',*,*,#1973,.F.);
#2653=ORIENTED_EDGE('',*,*,#1974,.F.);
#2654=ORIENTED_EDGE('',*,*,#1975,.T.);
#2655=ORIENTED_EDGE('',*,*,#1935,.T.);
#2656=ORIENTED_EDGE('',*,*,#1976,.F.);
#2657=ORIENTED_EDGE('',*,*,#1967,.T.);
#2658=ORIENTED_EDGE('',*,*,#1964,.T.);
#2659=ORIENTED_EDGE('',*,*,#1977,.T.);
#2660=ORIENTED_EDGE('',*,*,#1936,.F.);
#2661=ORIENTED_EDGE('',*,*,#1975,.F.);
#2662=ORIENTED_EDGE('',*,*,#1978,.F.);
#2663=ORIENTED_EDGE('',*,*,#1979,.F.);
#2664=ORIENTED_EDGE('',*,*,#1980,.T.);
#2665=ORIENTED_EDGE('',*,*,#1961,.T.);
#2666=ORIENTED_EDGE('',*,*,#1981,.F.);
#2667=ORIENTED_EDGE('',*,*,#1973,.T.);
#2668=ORIENTED_EDGE('',*,*,#1970,.T.);
#2669=ORIENTED_EDGE('',*,*,#1982,.T.);
#2670=ORIENTED_EDGE('',*,*,#1962,.F.);
#2671=ORIENTED_EDGE('',*,*,#1980,.F.);
#2672=ORIENTED_EDGE('',*,*,#1943,.F.);
#2673=ORIENTED_EDGE('',*,*,#1937,.F.);
#2674=ORIENTED_EDGE('',*,*,#1977,.F.);
#2675=ORIENTED_EDGE('',*,*,#1963,.F.);
#2676=ORIENTED_EDGE('',*,*,#1982,.F.);
#2677=ORIENTED_EDGE('',*,*,#1969,.F.);
#2678=ORIENTED_EDGE('',*,*,#1955,.F.);
#2679=ORIENTED_EDGE('',*,*,#1949,.F.);
#2680=ORIENTED_EDGE('',*,*,#1983,.T.);
#2681=ORIENTED_EDGE('',*,*,#1984,.T.);
#2682=ORIENTED_EDGE('',*,*,#1985,.T.);
#2683=ORIENTED_EDGE('',*,*,#1984,.F.);
#2684=ORIENTED_EDGE('',*,*,#1986,.T.);
#2685=ORIENTED_EDGE('',*,*,#1983,.F.);
#2686=ORIENTED_EDGE('',*,*,#1987,.F.);
#2687=ORIENTED_EDGE('',*,*,#1988,.T.);
#2688=ORIENTED_EDGE('',*,*,#1985,.F.);
#2689=ORIENTED_EDGE('',*,*,#1988,.F.);
#2690=ORIENTED_EDGE('',*,*,#1989,.F.);
#2691=ORIENTED_EDGE('',*,*,#1990,.T.);
#2692=ORIENTED_EDGE('',*,*,#1987,.T.);
#2693=ORIENTED_EDGE('',*,*,#1990,.F.);
#2694=ORIENTED_EDGE('',*,*,#1991,.F.);
#2695=ORIENTED_EDGE('',*,*,#1992,.T.);
#2696=ORIENTED_EDGE('',*,*,#1989,.T.);
#2697=ORIENTED_EDGE('',*,*,#1992,.F.);
#2698=ORIENTED_EDGE('',*,*,#1991,.T.);
#2699=ORIENTED_EDGE('',*,*,#1968,.T.);
#2700=ORIENTED_EDGE('',*,*,#1972,.T.);
#2701=ORIENTED_EDGE('',*,*,#1981,.T.);
#2702=ORIENTED_EDGE('',*,*,#1979,.T.);
#2703=ORIENTED_EDGE('',*,*,#1960,.T.);
#2704=ORIENTED_EDGE('',*,*,#1966,.T.);
#2705=ORIENTED_EDGE('',*,*,#1976,.T.);
#2706=ORIENTED_EDGE('',*,*,#1993,.T.);
#2707=ORIENTED_EDGE('',*,*,#1994,.F.);
#2708=ORIENTED_EDGE('',*,*,#1995,.F.);
#2709=ORIENTED_EDGE('',*,*,#1993,.F.);
#2710=ORIENTED_EDGE('',*,*,#1978,.T.);
#2711=ORIENTED_EDGE('',*,*,#1974,.T.);
#2712=ORIENTED_EDGE('',*,*,#1934,.T.);
#2713=ORIENTED_EDGE('',*,*,#1940,.T.);
#2714=ORIENTED_EDGE('',*,*,#1942,.T.);
#2715=ORIENTED_EDGE('',*,*,#1946,.T.);
#2716=ORIENTED_EDGE('',*,*,#1948,.T.);
#2717=ORIENTED_EDGE('',*,*,#1952,.T.);
#2718=ORIENTED_EDGE('',*,*,#1954,.T.);
#2719=ORIENTED_EDGE('',*,*,#1958,.T.);
#2720=ORIENTED_EDGE('',*,*,#1986,.F.);
#2721=ORIENTED_EDGE('',*,*,#1996,.T.);
#2722=ORIENTED_EDGE('',*,*,#1994,.T.);
#2723=ORIENTED_EDGE('',*,*,#1995,.T.);
#2724=ORIENTED_EDGE('',*,*,#1996,.F.);
#3191=CYLINDRICAL_SURFACE('',#3703,0.946);
#3192=CYLINDRICAL_SURFACE('',#3714,0.946);
#3193=CYLINDRICAL_SURFACE('',#3724,0.946);
#3194=CYLINDRICAL_SURFACE('',#3730,0.946);
#3195=CYLINDRICAL_SURFACE('',#3751,2.17846096908266);
#3196=CYLINDRICAL_SURFACE('',#3755,2.4505);
#3283=ADVANCED_FACE('',(#341),#3191,.T.);
#3284=ADVANCED_FACE('',(#342),#174,.F.);
#3285=ADVANCED_FACE('',(#343),#175,.F.);
#3286=ADVANCED_FACE('',(#344),#176,.F.);
#3287=ADVANCED_FACE('',(#345),#3192,.T.);
#3288=ADVANCED_FACE('',(#346),#177,.F.);
#3289=ADVANCED_FACE('',(#347),#178,.F.);
#3290=ADVANCED_FACE('',(#348),#179,.F.);
#3291=ADVANCED_FACE('',(#349),#3193,.T.);
#3292=ADVANCED_FACE('',(#350),#180,.F.);
#3293=ADVANCED_FACE('',(#351),#3194,.T.);
#3294=ADVANCED_FACE('',(#352),#181,.F.);
#3295=ADVANCED_FACE('',(#353),#182,.F.);
#3296=ADVANCED_FACE('',(#354),#183,.F.);
#3297=ADVANCED_FACE('',(#355),#184,.F.);
#3298=ADVANCED_FACE('',(#356),#185,.F.);
#3299=ADVANCED_FACE('',(#357),#186,.F.);
#3300=ADVANCED_FACE('',(#358),#128,.F.);
#3301=ADVANCED_FACE('',(#359,#110),#187,.T.);
#3302=ADVANCED_FACE('',(#360),#3195,.T.);
#3303=ADVANCED_FACE('',(#361),#105,.T.);
#3304=ADVANCED_FACE('',(#362),#3196,.T.);
#3305=ADVANCED_FACE('',(#363),#188,.T.);
#3306=ADVANCED_FACE('',(#364),#98,.T.);
#3307=ADVANCED_FACE('',(#365),#106,.T.);
#3400=CLOSED_SHELL('',(#3283,#3284,#3285,#3286,#3287,#3288,#3289,#3290,
#3291,#3292,#3293,#3294,#3295,#3296,#3297,#3298,#3299,#3300,#3301,#3302,
#3303,#3304,#3305,#3306,#3307));
#3702=AXIS2_PLACEMENT_3D('',#5493,#4332,#4333);
#3703=AXIS2_PLACEMENT_3D('',#5494,#4334,#4335);
#3704=AXIS2_PLACEMENT_3D('',#5515,#4337,#4338);
#3705=AXIS2_PLACEMENT_3D('',#5517,#4339,#4340);
#3706=AXIS2_PLACEMENT_3D('',#5519,#4341,#4342);
#3707=AXIS2_PLACEMENT_3D('',#5521,#4344,#4345);
#3708=AXIS2_PLACEMENT_3D('',#5523,#4346,#4347);
#3709=AXIS2_PLACEMENT_3D('',#5525,#4349,#4350);
#3710=AXIS2_PLACEMENT_3D('',#5527,#4351,#4352);
#3711=AXIS2_PLACEMENT_3D('',#5531,#4354,#4355);
#3712=AXIS2_PLACEMENT_3D('',#5533,#4357,#4358);
#3713=AXIS2_PLACEMENT_3D('',#5535,#4359,#4360);
#3714=AXIS2_PLACEMENT_3D('',#5537,#4362,#4363);
#3715=AXIS2_PLACEMENT_3D('',#5555,#4364,#4365);
#3716=AXIS2_PLACEMENT_3D('',#5557,#4366,#4367);
#3717=AXIS2_PLACEMENT_3D('',#5559,#4369,#4370);
#3718=AXIS2_PLACEMENT_3D('',#5561,#4371,#4372);
#3719=AXIS2_PLACEMENT_3D('',#5563,#4374,#4375);
#3720=AXIS2_PLACEMENT_3D('',#5565,#4376,#4377);
#3721=AXIS2_PLACEMENT_3D('',#5569,#4379,#4380);
#3722=AXIS2_PLACEMENT_3D('',#5571,#4382,#4383);
#3723=AXIS2_PLACEMENT_3D('',#5573,#4384,#4385);
#3724=AXIS2_PLACEMENT_3D('',#5575,#4387,#4388);
#3725=AXIS2_PLACEMENT_3D('',#5596,#4390,#4391);
#3726=AXIS2_PLACEMENT_3D('',#5598,#4392,#4393);
#3727=AXIS2_PLACEMENT_3D('',#5600,#4394,#4395);
#3728=AXIS2_PLACEMENT_3D('',#5602,#4397,#4398);
#3729=AXIS2_PLACEMENT_3D('',#5604,#4399,#4400);
#3730=AXIS2_PLACEMENT_3D('',#5606,#4402,#4403);
#3731=AXIS2_PLACEMENT_3D('',#5624,#4404,#4405);
#3732=AXIS2_PLACEMENT_3D('',#5626,#4406,#4407);
#3733=AXIS2_PLACEMENT_3D('',#5628,#4409,#4410);
#3734=AXIS2_PLACEMENT_3D('',#5630,#4411,#4412);
#3735=AXIS2_PLACEMENT_3D('',#5632,#4414,#4415);
#3736=AXIS2_PLACEMENT_3D('',#5634,#4416,#4417);
#3737=AXIS2_PLACEMENT_3D('',#5636,#4419,#4420);
#3738=AXIS2_PLACEMENT_3D('',#5638,#4421,#4422);
#3739=AXIS2_PLACEMENT_3D('',#5640,#4424,#4425);
#3740=AXIS2_PLACEMENT_3D('',#5641,#4426,#4427);
#3741=AXIS2_PLACEMENT_3D('',#5643,#4428,#4429);
#3742=AXIS2_PLACEMENT_3D('',#5645,#4431,#4432);
#3743=AXIS2_PLACEMENT_3D('',#5646,#4433,#4434);
#3744=AXIS2_PLACEMENT_3D('',#5648,#4436,#4437);
#3745=AXIS2_PLACEMENT_3D('',#5649,#4438,#4439);
#3746=AXIS2_PLACEMENT_3D('',#5651,#4440,#4441);
#3747=AXIS2_PLACEMENT_3D('',#5653,#4442,#4443);
#3748=AXIS2_PLACEMENT_3D('',#5654,#4444,#4445);
#3749=AXIS2_PLACEMENT_3D('',#5655,#4446,#4447);
#3750=AXIS2_PLACEMENT_3D('',#5657,#4448,#4449);
#3751=AXIS2_PLACEMENT_3D('',#5658,#4450,#4451);
#3752=AXIS2_PLACEMENT_3D('',#5660,#4452,#4453);
#3753=AXIS2_PLACEMENT_3D('',#5662,#4455,#4456);
#3754=AXIS2_PLACEMENT_3D('',#5664,#4457,#4458);
#3755=AXIS2_PLACEMENT_3D('',#5666,#4460,#4461);
#3756=AXIS2_PLACEMENT_3D('',#5668,#4462,#4463);
#3757=AXIS2_PLACEMENT_3D('',#5670,#4465,#4466);
#3758=AXIS2_PLACEMENT_3D('',#5671,#4467,#4468);
#3759=AXIS2_PLACEMENT_3D('',#5673,#4469,#4470);
#3760=AXIS2_PLACEMENT_3D('',#5675,#4471,#4472);
#3761=AXIS2_PLACEMENT_3D('',#5676,#4473,#4474);
#3762=AXIS2_PLACEMENT_3D('',#5677,#4475,#4476);
#4332=DIRECTION('axis',(0.,0.,1.));
#4333=DIRECTION('refdir',(1.,0.,0.));
#4334=DIRECTION('center_axis',(0.,0.,-1.));
#4335=DIRECTION('ref_axis',(0.707106781186563,-0.707106781186532,0.));
#4336=DIRECTION('',(0.,0.,1.));
#4337=DIRECTION('center_axis',(-0.866025403784439,0.,-0.5));
#4338=DIRECTION('ref_axis',(0.5,0.,-0.866025403784439));
#4339=DIRECTION('center_axis',(0.,0.,-1.));
#4340=DIRECTION('ref_axis',(0.707106781186563,-0.707106781186532,0.));
#4341=DIRECTION('center_axis',(-2.54091264057109E-15,0.866025403784439,
-0.5));
#4342=DIRECTION('ref_axis',(1.43032168209504E-15,-0.5,-0.866025403784439));
#4343=DIRECTION('',(0.,0.,-1.));
#4344=DIRECTION('center_axis',(-1.,-4.30300426108057E-14,0.));
#4345=DIRECTION('ref_axis',(-4.30300426108057E-14,1.,0.));
#4346=DIRECTION('center_axis',(-1.,-4.30300426108057E-14,0.));
#4347=DIRECTION('ref_axis',(0.,0.,-1.));
#4348=DIRECTION('',(-2.15150213054029E-14,0.5,0.866025403784439));
#4349=DIRECTION('center_axis',(-2.54091264057109E-15,0.866025403784439,
-0.5));
#4350=DIRECTION('ref_axis',(1.,2.93399319404209E-15,0.));
#4351=DIRECTION('center_axis',(-2.54091264057109E-15,0.866025403784439,
-0.5));
#4352=DIRECTION('ref_axis',(0.,-0.5,-0.866025403784439));
#4353=DIRECTION('',(-1.,-2.93399319404209E-15,0.));
#4354=DIRECTION('center_axis',(-2.54091264057109E-15,0.866025403784439,
-0.5));
#4355=DIRECTION('ref_axis',(1.46699659702056E-15,-0.5,-0.866025403784439));
#4356=DIRECTION('',(-1.73044443434865E-14,-0.5,-0.866025403784439));
#4357=DIRECTION('center_axis',(1.,-3.4608888686973E-14,0.));
#4358=DIRECTION('ref_axis',(-3.4608888686973E-14,-1.,0.));
#4359=DIRECTION('center_axis',(1.,-3.4608888686973E-14,0.));
#4360=DIRECTION('ref_axis',(0.,0.,1.));
#4361=DIRECTION('',(0.,0.,1.));
#4362=DIRECTION('center_axis',(0.,0.,-1.));
#4363=DIRECTION('ref_axis',(-0.707106781186546,-0.707106781186549,0.));
#4364=DIRECTION('center_axis',(0.,0.,-1.));
#4365=DIRECTION('ref_axis',(-0.707106781186546,-0.707106781186549,0.));
#4366=DIRECTION('center_axis',(0.866025403784439,0.,-0.5));
#4367=DIRECTION('ref_axis',(-0.5,-3.66749149255139E-17,-0.866025403784439));
#4368=DIRECTION('',(0.,0.,-1.));
#4369=DIRECTION('center_axis',(-4.04626176340286E-14,1.,0.));
#4370=DIRECTION('ref_axis',(1.,4.04626176340286E-14,0.));
#4371=DIRECTION('center_axis',(-4.04626176340286E-14,1.,0.));
#4372=DIRECTION('ref_axis',(0.,0.,-1.));
#4373=DIRECTION('',(0.5,2.02313088170143E-14,0.866025403784439));
#4374=DIRECTION('center_axis',(0.866025403784439,0.,-0.5));
#4375=DIRECTION('ref_axis',(0.,-1.,0.));
#4376=DIRECTION('center_axis',(0.866025403784439,0.,-0.5));
#4377=DIRECTION('ref_axis',(0.5,0.,0.866025403784439));
#4378=DIRECTION('',(0.,1.,0.));
#4379=DIRECTION('center_axis',(0.866025403784439,0.,-0.5));
#4380=DIRECTION('ref_axis',(-0.5,3.66749149255139E-17,-0.866025403784439));
#4381=DIRECTION('',(-0.5,2.39626331165986E-16,-0.866025403784439));
#4382=DIRECTION('center_axis',(-4.79252662331972E-16,-1.,0.));
#4383=DIRECTION('ref_axis',(-1.,4.79252662331972E-16,0.));
#4384=DIRECTION('center_axis',(-4.79252662331972E-16,-1.,0.));
#4385=DIRECTION('ref_axis',(0.,0.,1.));
#4386=DIRECTION('',(0.,0.,1.));
#4387=DIRECTION('center_axis',(0.,0.,-1.));
#4388=DIRECTION('ref_axis',(0.70710678118653,0.707106781186565,0.));
#4389=DIRECTION('',(0.,0.,1.));
#4390=DIRECTION('center_axis',(-1.27045632028555E-15,-0.866025403784439,
-0.5));
#4391=DIRECTION('ref_axis',(6.96823383584764E-16,0.5,-0.866025403784439));
#4392=DIRECTION('center_axis',(0.,0.,-1.));
#4393=DIRECTION('ref_axis',(0.70710678118653,0.707106781186565,0.));
#4394=DIRECTION('center_axis',(-0.866025403784439,0.,-0.5));
#4395=DIRECTION('ref_axis',(0.5,3.66749149255139E-17,-0.866025403784439));
#4396=DIRECTION('',(0.,0.,-1.));
#4397=DIRECTION('center_axis',(5.35736011821097E-14,-1.,0.));
#4398=DIRECTION('ref_axis',(-1.,-5.35736011821097E-14,0.));
#4399=DIRECTION('center_axis',(5.35736011821097E-14,-1.,0.));
#4400=DIRECTION('ref_axis',(0.,0.,1.));
#4401=DIRECTION('',(-0.5,-2.67868005910549E-14,0.866025403784439));
#4402=DIRECTION('center_axis',(0.,0.,-1.));
#4403=DIRECTION('ref_axis',(-0.707106781186557,0.707106781186538,0.));
#4404=DIRECTION('center_axis',(0.,0.,-1.));
#4405=DIRECTION('ref_axis',(-0.707106781186557,0.707106781186538,0.));
#4406=DIRECTION('center_axis',(-1.27045632028555E-15,-0.866025403784439,
-0.5));
#4407=DIRECTION('ref_axis',(7.33498298510278E-16,0.5,-0.866025403784439));
#4408=DIRECTION('',(0.,0.,-1.));
#4409=DIRECTION('center_axis',(1.,2.81047454124667E-14,0.));
#4410=DIRECTION('ref_axis',(2.81047454124667E-14,-1.,0.));
#4411=DIRECTION('center_axis',(1.,2.81047454124667E-14,0.));
#4412=DIRECTION('ref_axis',(0.,0.,1.));
#4413=DIRECTION('',(1.40523727062334E-14,-0.5,0.866025403784439));
#4414=DIRECTION('center_axis',(0.,1.,0.));
#4415=DIRECTION('ref_axis',(1.,0.,0.));
#4416=DIRECTION('center_axis',(0.,1.,0.));
#4417=DIRECTION('ref_axis',(0.,0.,-1.));
#4418=DIRECTION('',(0.5,0.,-0.866025403784439));
#4419=DIRECTION('center_axis',(-0.866025403784439,0.,-0.5));
#4420=DIRECTION('ref_axis',(0.,1.,0.));
#4421=DIRECTION('center_axis',(-0.866025403784439,0.,-0.5));
#4422=DIRECTION('ref_axis',(0.5,0.,-0.866025403784439));
#4423=DIRECTION('',(0.,-1.,0.));
#4424=DIRECTION('center_axis',(-0.866025403784439,0.,-0.5));
#4425=DIRECTION('ref_axis',(0.5,0.,-0.866025403784439));
#4426=DIRECTION('center_axis',(-1.,3.8682536316795E-15,0.));
#4427=DIRECTION('ref_axis',(3.8682536316795E-15,1.,0.));
#4428=DIRECTION('center_axis',(-1.,3.8682536316795E-15,0.));
#4429=DIRECTION('ref_axis',(0.,0.,-1.));
#4430=DIRECTION('',(1.93412681583975E-15,0.5,-0.866025403784439));
#4431=DIRECTION('center_axis',(-1.27045632028555E-15,-0.866025403784439,
-0.5));
#4432=DIRECTION('ref_axis',(-1.,1.46699659702105E-15,0.));
#4433=DIRECTION('center_axis',(-1.27045632028555E-15,-0.866025403784439,
-0.5));
#4434=DIRECTION('ref_axis',(0.,-0.5,0.866025403784439));
#4435=DIRECTION('',(1.,-1.46699659702105E-15,0.));
#4436=DIRECTION('center_axis',(0.,0.,-1.));
#4437=DIRECTION('ref_axis',(-1.,0.,0.));
#4438=DIRECTION('center_axis',(0.,0.,-1.));
#4439=DIRECTION('ref_axis',(-1.,0.,0.));
#4440=DIRECTION('center_axis',(0.,0.,-1.));
#4441=DIRECTION('ref_axis',(1.,0.,0.));
#4442=DIRECTION('center_axis',(-1.22464679914735E-16,-1.,0.));
#4443=DIRECTION('ref_axis',(1.,-1.22464679914735E-16,0.));
#4444=DIRECTION('center_axis',(0.,0.,1.));
#4445=DIRECTION('ref_axis',(1.,0.,0.));
#4446=DIRECTION('center_axis',(0.,0.,-1.));
#4447=DIRECTION('ref_axis',(-1.,0.,0.));
#4448=DIRECTION('center_axis',(0.,0.,-1.));
#4449=DIRECTION('ref_axis',(1.,0.,0.));
#4450=DIRECTION('center_axis',(0.,0.,-1.));
#4451=DIRECTION('ref_axis',(-1.,0.,0.));
#4452=DIRECTION('center_axis',(0.,0.,-1.));
#4453=DIRECTION('ref_axis',(1.,0.,0.));
#4454=DIRECTION('',(0.,0.,1.));
#4455=DIRECTION('center_axis',(0.,0.,-1.));
#4456=DIRECTION('ref_axis',(-1.,0.,0.));
#4457=DIRECTION('center_axis',(0.,0.,-1.));
#4458=DIRECTION('ref_axis',(-1.,0.,0.));
#4459=DIRECTION('',(-0.258819045102519,3.16961915143174E-17,0.965925826289069));
#4460=DIRECTION('center_axis',(0.,0.,-1.));
#4461=DIRECTION('ref_axis',(-1.,0.,0.));
#4462=DIRECTION('center_axis',(0.,0.,1.));
#4463=DIRECTION('ref_axis',(-1.,0.,0.));
#4464=DIRECTION('',(0.,0.,1.));
#4465=DIRECTION('center_axis',(0.,0.,-1.));
#4466=DIRECTION('ref_axis',(-1.,0.,0.));
#4467=DIRECTION('center_axis',(6.12323399573676E-17,0.,1.));
#4468=DIRECTION('ref_axis',(1.,0.,0.));
#4469=DIRECTION('center_axis',(1.22464679914735E-16,-1.,0.));
#4470=DIRECTION('ref_axis',(-1.,-1.22464679914735E-16,0.));
#4471=DIRECTION('center_axis',(0.,0.,-1.));
#4472=DIRECTION('ref_axis',(1.,0.,0.));
#4473=DIRECTION('center_axis',(0.,0.,-1.));
#4474=DIRECTION('ref_axis',(1.,0.,0.));
#4475=DIRECTION('center_axis',(0.,0.,-1.));
#4476=DIRECTION('ref_axis',(-1.,0.,0.));
#4477=DIRECTION('',(-0.0871557427578718,1.06735001395738E-17,0.996194698090852));
#5493=CARTESIAN_POINT('',(0.,0.,0.));
#5494=CARTESIAN_POINT('Origin',(-1.41899999999985,1.41899999999965,3.1));
#5495=CARTESIAN_POINT('',(-1.41899999999985,0.472999999999654,3.01252522110193));
#5496=CARTESIAN_POINT('',(-0.472999999999848,1.41899999999969,3.01252522110194));
#5497=CARTESIAN_POINT('Ctrl Pts',(-1.41899999999985,0.472999999999654,3.01252522110193));
#5498=CARTESIAN_POINT('Ctrl Pts',(-1.418237843063,0.472999999999654,3.01261008153857));
#5499=CARTESIAN_POINT('Ctrl Pts',(-1.41747599318127,0.473000921064105,3.01269480438576));
#5500=CARTESIAN_POINT('Ctrl Pts',(-1.29873656917598,0.473287797471327,3.02588334070707));
#5501=CARTESIAN_POINT('Ctrl Pts',(-1.17260477262757,0.497030428020145,3.03726209636997));
#5502=CARTESIAN_POINT('Ctrl Pts',(-0.940241249793281,0.593452559529333,
3.05235989856665));
#5503=CARTESIAN_POINT('Ctrl Pts',(-0.834013199901804,0.666140770092746,
3.05607990145755));
#5504=CARTESIAN_POINT('Ctrl Pts',(-0.75007698499736,0.750076984997194,3.05607990145756));
#5505=CARTESIAN_POINT('Ctrl Pts',(-0.666140770092915,0.834013199901643,
3.05607990145756));
#5506=CARTESIAN_POINT('Ctrl Pts',(-0.593452559529506,0.940241249793123,
3.05235989856665));
#5507=CARTESIAN_POINT('Ctrl Pts',(-0.497030428020328,1.17260477262741,3.03726209636997));
#5508=CARTESIAN_POINT('Ctrl Pts',(-0.473287797471517,1.29873656917583,3.02588334070708));
#5509=CARTESIAN_POINT('Ctrl Pts',(-0.4730009210643,1.41747599318095,3.01269480438579));
#5510=CARTESIAN_POINT('Ctrl Pts',(-0.472999999999848,1.41823784306269,3.0126100815386));
#5511=CARTESIAN_POINT('Ctrl Pts',(-0.472999999999848,1.41899999999969,3.01252522110194));
#5512=CARTESIAN_POINT('',(-1.41899999999985,0.472999999999654,1.22765307701778));
#5513=CARTESIAN_POINT('',(-1.41899999999985,0.472999999999654,3.1));
#5514=CARTESIAN_POINT('',(-0.866098738193358,0.651395808574938,0.27));
#5515=CARTESIAN_POINT('Origin',(-1.41899999999985,1.41899999999965,1.22765307701778));
#5516=CARTESIAN_POINT('',(-0.651395808574991,0.86609873819336,0.27));
#5517=CARTESIAN_POINT('Origin',(-1.41899999999985,1.41899999999965,0.27));
#5518=CARTESIAN_POINT('',(-0.472999999999848,1.41899999999969,1.22765307701751));
#5519=CARTESIAN_POINT('Origin',(-1.41899999999985,1.41899999999965,1.22765307701745));
#5520=CARTESIAN_POINT('',(-0.472999999999848,1.41899999999969,3.1));
#5521=CARTESIAN_POINT('Origin',(-0.472999999999807,0.472999999999754,3.1));
#5522=CARTESIAN_POINT('',(-0.472999999999889,2.36767196216383,2.87080111520185));
#5523=CARTESIAN_POINT('Origin',(-0.472999999999787,-2.0353210154902E-14,
-9.73193776093083));
#5524=CARTESIAN_POINT('',(-0.472999999999884,2.24662499999997,2.66114162663218));
#5525=CARTESIAN_POINT('Origin',(-0.472999999999895,2.5,3.1));
#5526=CARTESIAN_POINT('',(0.472999999999787,2.36767196216383,2.87080111520185));
#5527=CARTESIAN_POINT('Origin',(1.16338464595253E-14,-3.68139204037345,
-7.60648507542867));
#5528=CARTESIAN_POINT('',(0.651395808575038,0.866098738193364,0.27));
#5529=CARTESIAN_POINT('',(-0.236499999999946,0.866098738193362,0.27));
#5530=CARTESIAN_POINT('',(0.472999999999754,1.41899999999989,1.22765307701784));
#5531=CARTESIAN_POINT('Origin',(1.41899999999975,1.41899999999985,1.22765307701778));
#5532=CARTESIAN_POINT('',(0.472999999999791,2.5,3.09999999999999));
#5533=CARTESIAN_POINT('Origin',(0.472999999999791,2.5,3.1));
#5534=CARTESIAN_POINT('',(0.472999999999754,1.41899999999989,3.01252522110192));
#5535=CARTESIAN_POINT('Origin',(0.472999999999705,-1.6370004348928E-14,
-9.73193776093083));
#5536=CARTESIAN_POINT('',(0.472999999999754,1.41899999999989,3.1));
#5537=CARTESIAN_POINT('Origin',(1.41899999999975,1.41899999999985,3.1));
#5538=CARTESIAN_POINT('',(1.41899999999979,0.472999999999854,3.01252522110193));
#5539=CARTESIAN_POINT('Ctrl Pts',(0.472999999999754,1.41899999999989,3.01252522110192));
#5540=CARTESIAN_POINT('Ctrl Pts',(0.472999999999754,1.41823784306304,3.01261008153856));
#5541=CARTESIAN_POINT('Ctrl Pts',(0.473000921064206,1.4174759931813,3.01269480438575));
#5542=CARTESIAN_POINT('Ctrl Pts',(0.473287797471426,1.29873656917601,3.02588334070706));
#5543=CARTESIAN_POINT('Ctrl Pts',(0.49703042802024,1.17260477262759,3.03726209636996));
#5544=CARTESIAN_POINT('Ctrl Pts',(0.593452559529424,0.940241249793303,3.05235989856665));
#5545=CARTESIAN_POINT('Ctrl Pts',(0.666140770092836,0.834013199901824,3.05607990145755));
#5546=CARTESIAN_POINT('Ctrl Pts',(0.750076984997282,0.750076984997378,3.05607990145755));
#5547=CARTESIAN_POINT('Ctrl Pts',(0.834013199901729,0.666140770092932,3.05607990145755));
#5548=CARTESIAN_POINT('Ctrl Pts',(0.940241249793208,0.593452559529521,3.05235989856665));
#5549=CARTESIAN_POINT('Ctrl Pts',(1.1726047726275,0.497030428020338,3.03726209636996));
#5550=CARTESIAN_POINT('Ctrl Pts',(1.29873656917591,0.473287797471525,3.02588334070707));
#5551=CARTESIAN_POINT('Ctrl Pts',(1.41747599318104,0.473000921064306,3.01269480438578));
#5552=CARTESIAN_POINT('Ctrl Pts',(1.41823784306278,0.472999999999854,3.01261008153858));
#5553=CARTESIAN_POINT('Ctrl Pts',(1.41899999999979,0.472999999999854,3.01252522110193));
#5554=CARTESIAN_POINT('',(0.866098738193361,0.651395808575069,0.27));
#5555=CARTESIAN_POINT('Origin',(1.41899999999975,1.41899999999985,0.27));
#5556=CARTESIAN_POINT('',(1.41899999999979,0.472999999999853,1.22765307701768));
#5557=CARTESIAN_POINT('Origin',(1.41899999999975,1.41899999999985,1.22765307701762));
#5558=CARTESIAN_POINT('',(1.41899999999979,0.472999999999854,3.1));
#5559=CARTESIAN_POINT('Origin',(0.472999999999817,0.472999999999815,3.1));
#5560=CARTESIAN_POINT('',(2.36767196216383,0.472999999999892,2.87080111520185));
#5561=CARTESIAN_POINT('Origin',(-1.83061508724184E-14,0.472999999999796,
-9.73193776093083));
#5562=CARTESIAN_POINT('',(2.24662499999998,0.472999999999887,2.6611416266322));
#5563=CARTESIAN_POINT('Origin',(2.5,0.472999999999897,3.1));
#5564=CARTESIAN_POINT('',(2.36767196216383,-0.472999999999786,2.87080111520185));
#5565=CARTESIAN_POINT('Origin',(-3.68139204037345,0.,-7.60648507542867));
#5566=CARTESIAN_POINT('',(0.866098738193361,-0.65139580857508,0.270000000000001));
#5567=CARTESIAN_POINT('',(0.86609873819336,0.236499999999951,0.27));
#5568=CARTESIAN_POINT('',(1.41899999999987,-0.472999999999785,1.22765307701781));
#5569=CARTESIAN_POINT('Origin',(1.41899999999987,-1.41899999999979,1.22765307701781));
#5570=CARTESIAN_POINT('',(2.5,-0.472999999999786,3.1));
#5571=CARTESIAN_POINT('Origin',(2.5,-0.472999999999786,3.1));
#5572=CARTESIAN_POINT('',(1.41899999999987,-0.472999999999785,3.01252522110192));
#5573=CARTESIAN_POINT('Origin',(6.05980759185948E-16,-0.472999999999784,
-9.73193776093083));
#5574=CARTESIAN_POINT('',(1.41899999999987,-0.472999999999785,3.1));
#5575=CARTESIAN_POINT('Origin',(-1.41899999999978,-1.41899999999983,3.1));
#5576=CARTESIAN_POINT('',(-0.472999999999784,-1.41899999999984,3.01252522110192));
#5577=CARTESIAN_POINT('',(-1.41899999999983,-0.472999999999835,3.01252522110192));
#5578=CARTESIAN_POINT('Ctrl Pts',(-0.472999999999784,-1.41899999999984,
3.01252522110192));
#5579=CARTESIAN_POINT('Ctrl Pts',(-0.472999999999784,-1.41823784306299,
3.01261008153856));
#5580=CARTESIAN_POINT('Ctrl Pts',(-0.473000921064235,-1.41747599318126,
3.01269480438576));
#5581=CARTESIAN_POINT('Ctrl Pts',(-0.473287797471458,-1.29873656917597,
3.02588334070707));
#5582=CARTESIAN_POINT('Ctrl Pts',(-0.497030428020275,-1.17260477262755,
3.03726209636996));
#5583=CARTESIAN_POINT('Ctrl Pts',(-0.593452559529464,-0.940241249793266,
3.05235989856664));
#5584=CARTESIAN_POINT('Ctrl Pts',(-0.666140770092878,-0.834013199901788,
3.05607990145755));
#5585=CARTESIAN_POINT('Ctrl Pts',(-0.750076984997327,-0.750076984997344,
3.05607990145755));
#5586=CARTESIAN_POINT('Ctrl Pts',(-0.834013199901775,-0.6661407700929,3.05607990145755));
#5587=CARTESIAN_POINT('Ctrl Pts',(-0.940241249793256,-0.593452559529491,
3.05235989856665));
#5588=CARTESIAN_POINT('Ctrl Pts',(-1.17260477262755,-0.497030428020314,
3.03726209636996));
#5589=CARTESIAN_POINT('Ctrl Pts',(-1.29873656917596,-0.473287797471503,
3.02588334070706));
#5590=CARTESIAN_POINT('Ctrl Pts',(-1.41747599318109,-0.473000921064287,
3.01269480438577));
#5591=CARTESIAN_POINT('Ctrl Pts',(-1.41823784306282,-0.472999999999835,
3.01261008153858));
#5592=CARTESIAN_POINT('Ctrl Pts',(-1.41899999999983,-0.472999999999835,
3.01252522110192));
#5593=CARTESIAN_POINT('',(-0.472999999999784,-1.41899999999984,1.22765307701777));
#5594=CARTESIAN_POINT('',(-0.472999999999784,-1.41899999999984,3.1));
#5595=CARTESIAN_POINT('',(-0.651395808575061,-0.866098738193354,0.27));
#5596=CARTESIAN_POINT('Origin',(-1.41899999999978,-1.41899999999983,1.22765307701777));
#5597=CARTESIAN_POINT('',(-0.866098738193358,-0.651395808575073,0.27));
#5598=CARTESIAN_POINT('Origin',(-1.41899999999978,-1.41899999999983,0.27));
#5599=CARTESIAN_POINT('',(-1.41899999999983,-0.472999999999835,1.22765307701776));
#5600=CARTESIAN_POINT('Origin',(-1.41899999999978,-1.41899999999983,1.22765307701767));
#5601=CARTESIAN_POINT('',(-1.41899999999983,-0.472999999999835,3.1));
#5602=CARTESIAN_POINT('Origin',(-0.472999999999781,-0.472999999999784,3.1));
#5603=CARTESIAN_POINT('',(-2.36767196216382,-0.472999999999886,2.87080111520185));
#5604=CARTESIAN_POINT('Origin',(2.61729806275939E-14,-0.472999999999759,
-9.73193776093083));
#5605=CARTESIAN_POINT('',(-2.24662499999997,-0.472999999999879,2.66114162663219));
#5606=CARTESIAN_POINT('Origin',(1.41899999999987,-1.41899999999979,3.1));
#5607=CARTESIAN_POINT('',(0.472999999999865,-1.41899999999981,3.01252522110192));
#5608=CARTESIAN_POINT('Ctrl Pts',(1.41899999999987,-0.472999999999785,3.01252522110192));
#5609=CARTESIAN_POINT('Ctrl Pts',(1.41823784306302,-0.472999999999785,3.01261008153856));
#5610=CARTESIAN_POINT('Ctrl Pts',(1.41747599318129,-0.473000921064237,3.01269480438575));
#5611=CARTESIAN_POINT('Ctrl Pts',(1.29873656917601,-0.473287797471458,3.02588334070706));
#5612=CARTESIAN_POINT('Ctrl Pts',(1.17260477262759,-0.497030428020274,3.03726209636996));
#5613=CARTESIAN_POINT('Ctrl Pts',(0.940241249793305,-0.59345255952946,3.05235989856664));
#5614=CARTESIAN_POINT('Ctrl Pts',(0.834013199901827,-0.666140770092873,
3.05607990145755));
#5615=CARTESIAN_POINT('Ctrl Pts',(0.750076984997382,-0.75007698499732,3.05607990145755));
#5616=CARTESIAN_POINT('Ctrl Pts',(0.666140770092937,-0.834013199901768,
3.05607990145755));
#5617=CARTESIAN_POINT('Ctrl Pts',(0.593452559529527,-0.940241249793248,
3.05235989856665));
#5618=CARTESIAN_POINT('Ctrl Pts',(0.497030428020347,-1.17260477262754,3.03726209636996));
#5619=CARTESIAN_POINT('Ctrl Pts',(0.473287797471535,-1.29873656917595,3.02588334070706));
#5620=CARTESIAN_POINT('Ctrl Pts',(0.473000921064317,-1.41747599318107,3.01269480438577));
#5621=CARTESIAN_POINT('Ctrl Pts',(0.472999999999865,-1.4182378430628,3.01261008153858));
#5622=CARTESIAN_POINT('Ctrl Pts',(0.472999999999865,-1.41899999999981,3.01252522110192));
#5623=CARTESIAN_POINT('',(0.651395808575106,-0.866098738193356,0.27));
#5624=CARTESIAN_POINT('Origin',(1.41899999999987,-1.41899999999979,0.27));
#5625=CARTESIAN_POINT('',(0.472999999999865,-1.41899999999981,1.22765307701772));
#5626=CARTESIAN_POINT('Origin',(1.41899999999987,-1.41899999999979,1.22765307701768));
#5627=CARTESIAN_POINT('',(0.472999999999865,-1.41899999999981,3.1));
#5628=CARTESIAN_POINT('Origin',(0.472999999999839,-0.472999999999785,3.1));
#5629=CARTESIAN_POINT('',(0.472999999999892,-2.36767196216382,2.87080111520185));
#5630=CARTESIAN_POINT('Origin',(0.472999999999825,1.32935445800918E-14,
-9.73193776093083));
#5631=CARTESIAN_POINT('',(0.472999999999889,-2.24662499999997,2.66114162663219));
#5632=CARTESIAN_POINT('Origin',(-2.5,0.472999999999654,3.1));
#5633=CARTESIAN_POINT('',(-2.36767196216383,0.472999999999654,2.87080111520186));
#5634=CARTESIAN_POINT('Origin',(8.32667268468867E-16,0.472999999999654,
-9.73193776093083));
#5635=CARTESIAN_POINT('',(-2.5,0.472999999999654,3.1));
#5636=CARTESIAN_POINT('Origin',(-2.5,-0.472999999999893,3.1));
#5637=CARTESIAN_POINT('',(-2.37229341204248,-2.90522153369617E-16,2.87880570119631));
#5638=CARTESIAN_POINT('Origin',(3.68139204037345,0.,-7.60648507542867));
#5639=CARTESIAN_POINT('',(-0.866098738193358,-0.236499999999945,0.27));
#5640=CARTESIAN_POINT('Origin',(3.68139204037345,0.,-7.60648507542867));
#5641=CARTESIAN_POINT('Origin',(-0.472999999999788,-2.5,3.1));
#5642=CARTESIAN_POINT('',(-0.472999999999788,-2.36767196216382,2.87080111520185));
#5643=CARTESIAN_POINT('Origin',(-0.472999999999779,1.82968396778355E-15,
-9.73193776093083));
#5644=CARTESIAN_POINT('',(-0.472999999999788,-2.5,3.1));
#5645=CARTESIAN_POINT('Origin',(0.472999999999896,-2.5,3.1));
#5646=CARTESIAN_POINT('Origin',(6.23325686399709E-15,3.68139204037346,-7.60648507542867));
#5647=CARTESIAN_POINT('',(0.236499999999949,-0.866098738193356,0.27));
#5648=CARTESIAN_POINT('Origin',(1.11022302462516E-15,3.88578058618805E-15,
0.27));
#5649=CARTESIAN_POINT('Origin',(0.,0.,-0.2));
#5650=CARTESIAN_POINT('',(2.37846096908266,-2.91277461268399E-16,-3.46944695195361E-17));
#5651=CARTESIAN_POINT('Origin',(0.,0.,-3.46944695195361E-17));
#5652=CARTESIAN_POINT('',(2.17846096908266,-2.66784525285452E-16,-0.2));
#5653=CARTESIAN_POINT('Origin',(2.37846096908266,-2.91277461268399E-16,
-0.2));
#5654=CARTESIAN_POINT('Origin',(0.,0.,-0.2));
#5655=CARTESIAN_POINT('Origin',(-2.17846096908266,0.,-1.88141750998334E-17));
#5656=CARTESIAN_POINT('',(5.15,-6.30693101560887E-16,-2.77555756156289E-16));
#5657=CARTESIAN_POINT('Origin',(0.,0.,0.));
#5658=CARTESIAN_POINT('Origin',(0.,0.,-0.149999999999999));
#5659=CARTESIAN_POINT('',(2.17846096908266,-2.66784525285452E-16,-0.299999999999998));
#5660=CARTESIAN_POINT('Origin',(0.,0.,-0.299999999999998));
#5661=CARTESIAN_POINT('',(2.17846096908266,-2.66784525285452E-16,-0.149999999999999));
#5662=CARTESIAN_POINT('Origin',(0.,0.,-0.899999999999999));
#5663=CARTESIAN_POINT('',(2.4505,-3.00099698131059E-16,-1.31526348502534));
#5664=CARTESIAN_POINT('Origin',(0.,0.,-1.31526348502534));
#5665=CARTESIAN_POINT('',(2.33923048454133,-2.86473112536145E-16,-0.899999999999999));
#5666=CARTESIAN_POINT('Origin',(0.,0.,-7.75));
#5667=CARTESIAN_POINT('',(2.4505,3.00099698131059E-16,-14.));
#5668=CARTESIAN_POINT('Origin',(0.,0.,-14.));
#5669=CARTESIAN_POINT('',(2.4505,-3.00099698131059E-16,-7.75));
#5670=CARTESIAN_POINT('Origin',(0.,0.,-14.));
#5671=CARTESIAN_POINT('Origin',(8.32667268468867E-16,0.,-9.73193776093083));
#5672=CARTESIAN_POINT('',(-4.96627380657387,0.,2.1));
#5673=CARTESIAN_POINT('Origin',(8.32667268468867E-16,0.,-9.73193776093083));
#5674=CARTESIAN_POINT('',(4.96627380657386,-6.08193132091002E-16,2.1));
#5675=CARTESIAN_POINT('Origin',(0.,0.,2.1));
#5676=CARTESIAN_POINT('Origin',(0.,0.,2.1));
#5677=CARTESIAN_POINT('Origin',(0.,0.,1.05));
#5678=CARTESIAN_POINT('',(5.05813690328693,-6.19443116825945E-16,1.05));
#7028=UNCERTAINTY_MEASURE_WITH_UNIT(LENGTH_MEASURE(0.01),#7048,
'DISTANCE_ACCURACY_VALUE',
'Maximum model space distance between geometric entities at asserted c
onnectivities');
#7035=UNCERTAINTY_MEASURE_WITH_UNIT(LENGTH_MEASURE(0.01),#7048,
'DISTANCE_ACCURACY_VALUE',
'Maximum model space distance between geometric entities at asserted c
onnectivities');
#7040=(
GEOMETRIC_REPRESENTATION_CONTEXT(3)
GLOBAL_UNCERTAINTY_ASSIGNED_CONTEXT((#7028))
GLOBAL_UNIT_ASSIGNED_CONTEXT((#7048,#7050,#7051))
REPRESENTATION_CONTEXT('','3D')
);
#7047=(
GEOMETRIC_REPRESENTATION_CONTEXT(3)
GLOBAL_UNCERTAINTY_ASSIGNED_CONTEXT((#7035))
GLOBAL_UNIT_ASSIGNED_CONTEXT((#7048,#7050,#7051))
REPRESENTATION_CONTEXT('','3D')
);
#7048=(
LENGTH_UNIT()
NAMED_UNIT(*)
SI_UNIT(.MILLI.,.METRE.)
);
#7050=(
NAMED_UNIT(*)
PLANE_ANGLE_UNIT()
SI_UNIT($,.RADIAN.)
);
#7051=(
NAMED_UNIT(*)
SI_UNIT($,.STERADIAN.)
SOLID_ANGLE_UNIT()
);
#7056=SHAPE_DEFINITION_REPRESENTATION(#7067,#7088);
#7067=PRODUCT_DEFINITION_SHAPE('',$,#7100);
#7088=SHAPE_REPRESENTATION('',(#3702),#7040);
#7095=PRODUCT_DEFINITION_CONTEXT('part definition',#7130,'design');
#7100=PRODUCT_DEFINITION('BHS JIS B 1111 - M5x14 Steel 4.6 Plain_3',
'M5x14 Steel 4.6 Plain v1 (3)',#7111,#7095);
#7111=PRODUCT_DEFINITION_FORMATION('',$,#7136);
#7130=APPLICATION_CONTEXT(
'Core Data for Automotive Mechanical Design Process');
#7131=PRODUCT_CONTEXT('part definition',#7130,'mechanical');
#7136=PRODUCT('BHS JIS B 1111 - M5x14 Steel 4.6 Plain_3',
'M5x14 Steel 4.6 Plain v1 (3)','Binding Head Screw JIS B 1111 - M5x14',
(#7131));
#7206=COLOUR_RGB('Off White',0.89,0.88,0.83);
#7207=FILL_AREA_STYLE_COLOUR('',#7206);
#7208=FILL_AREA_STYLE('',(#7207));
#7209=SURFACE_STYLE_FILL_AREA(#7208);
#7210=SURFACE_SIDE_STYLE('',(#7209));
#7211=SURFACE_STYLE_USAGE(.BOTH.,#7210);
#7212=PRESENTATION_STYLE_ASSIGNMENT((#7211));
ENDSEC;
END-ISO-10303-21;
